ISO-10303-21;
HEADER;
/* Generated by software containing ST-Developer
 * from STEP Tools, Inc. (www.steptools.com) 
 */

FILE_DESCRIPTION(
/* description */ ('PAT-072'),
/* implementation_level */ '2;1');

FILE_NAME(
/* name */ 'M2 sight screw (1).step',
/* time_stamp */ '2026-10-29T20:11:56-07:00',
/* author */ (''),
/* organization */ (''),
/* preprocessor_version */ 'ST-DEVELOPER v20.2',
/* originating_system */ 'Autodesk Translation Framework v15.17.0.0',
/* authorisation */ '');

FILE_SCHEMA (('AUTOMOTIVE_DESIGN { 1 0 10303 214 3 1 1 }'));
ENDSEC;

DATA;
#10=MECHANICAL_DESIGN_GEOMETRIC_PRESENTATION_REPRESENTATION('',(#355),#11432);
#283=SHAPE_REPRESENTATION_RELATIONSHIP('SRR','None',#11587,#319);
#319=ADVANCED_BREP_SHAPE_REPRESENTATION('',(#391),#11418);
#355=STYLED_ITEM('',(#11826),#391);
#391=MANIFOLD_SOLID_BREP('Body1',#6090);
#529=FACE_BOUND('',#1541,.T.);
#709=PLANE('',#6971);
#710=PLANE('',#6972);
#711=PLANE('',#6973);
#712=PLANE('',#6976);
#713=PLANE('',#6978);
#714=PLANE('',#6981);
#715=PLANE('',#6987);
#1036=FACE_OUTER_BOUND('',#1535,.T.);
#1037=FACE_OUTER_BOUND('',#1536,.T.);
#1038=FACE_OUTER_BOUND('',#1537,.T.);
#1039=FACE_OUTER_BOUND('',#1538,.T.);
#1040=FACE_OUTER_BOUND('',#1539,.T.);
#1041=FACE_OUTER_BOUND('',#1540,.T.);
#1042=FACE_OUTER_BOUND('',#1542,.T.);
#1043=FACE_OUTER_BOUND('',#1543,.T.);
#1044=FACE_OUTER_BOUND('',#1544,.T.);
#1535=EDGE_LOOP('',(#5042,#5043,#5044,#5045));
#1536=EDGE_LOOP('',(#5046,#5047,#5048,#5049));
#1537=EDGE_LOOP('',(#5050,#5051,#5052,#5053));
#1538=EDGE_LOOP('',(#5054,#5055));
#1539=EDGE_LOOP('',(#5056,#5057,#5058));
#1540=EDGE_LOOP('',(#5059));
#1541=EDGE_LOOP('',(#5060));
#1542=EDGE_LOOP('',(#5061,#5062,#5063,#5064,#5065,#5066,#5067,#5068,#5069,
#5070,#5071,#5072));
#1543=EDGE_LOOP('',(#5073,#5074,#5075,#5076));
#1544=EDGE_LOOP('',(#5077));
#1962=LINE('',#10736,#2381);
#1963=LINE('',#10738,#2382);
#1964=LINE('',#10740,#2383);
#1965=LINE('',#10741,#2384);
#1966=LINE('',#10745,#2385);
#1967=LINE('',#10747,#2386);
#1968=LINE('',#10749,#2387);
#1969=LINE('',#10750,#2388);
#1970=LINE('',#10766,#2389);
#1971=LINE('',#10770,#2390);
#2381=VECTOR('',#8453,1.);
#2382=VECTOR('',#8454,1.);
#2383=VECTOR('',#8455,1.);
#2384=VECTOR('',#8456,1.);
#2385=VECTOR('',#8459,1.);
#2386=VECTOR('',#8460,1.);
#2387=VECTOR('',#8461,1.);
#2388=VECTOR('',#8462,1.);
#2389=VECTOR('',#8487,0.175);
#2390=VECTOR('',#8492,0.1);
#2743=CIRCLE('',#6974,0.175);
#2744=CIRCLE('',#6975,0.175);
#2745=CIRCLE('',#6977,0.175);
#2746=CIRCLE('',#6979,0.175);
#2747=CIRCLE('',#6980,0.175);
#2748=CIRCLE('',#6982,0.175);
#2749=CIRCLE('',#6983,0.1);
#2750=CIRCLE('',#6986,0.1);
#3154=VERTEX_POINT('',#10734);
#3155=VERTEX_POINT('',#10735);
#3156=VERTEX_POINT('',#10737);
#3157=VERTEX_POINT('',#10739);
#3158=VERTEX_POINT('',#10743);
#3159=VERTEX_POINT('',#10744);
#3160=VERTEX_POINT('',#10746);
#3161=VERTEX_POINT('',#10748);
#3162=VERTEX_POINT('',#10757);
#3163=VERTEX_POINT('',#10761);
#3164=VERTEX_POINT('',#10763);
#3165=VERTEX_POINT('',#10768);
#3810=EDGE_CURVE('',#3154,#3155,#1962,.T.);
#3811=EDGE_CURVE('',#3154,#3156,#1963,.T.);
#3812=EDGE_CURVE('',#3157,#3156,#1964,.T.);
#3813=EDGE_CURVE('',#3155,#3157,#1965,.T.);
#3814=EDGE_CURVE('',#3158,#3159,#1966,.T.);
#3815=EDGE_CURVE('',#3160,#3158,#1967,.T.);
#3816=EDGE_CURVE('',#3161,#3160,#1968,.T.);
#3817=EDGE_CURVE('',#3161,#3159,#1969,.T.);
#3818=EDGE_CURVE('',#3159,#3154,#2743,.T.);
#3819=EDGE_CURVE('',#3156,#3161,#2744,.T.);
#3820=EDGE_CURVE('',#3160,#3158,#2745,.T.);
#3821=EDGE_CURVE('',#3162,#3157,#2746,.T.);
#3822=EDGE_CURVE('',#3155,#3162,#2747,.T.);
#3823=EDGE_CURVE('',#3163,#3163,#2748,.T.);
#3824=EDGE_CURVE('',#3164,#3164,#2749,.T.);
#3825=EDGE_CURVE('',#3163,#3162,#1970,.T.);
#3826=EDGE_CURVE('',#3165,#3165,#2750,.T.);
#3827=EDGE_CURVE('',#3165,#3164,#1971,.T.);
#5042=ORIENTED_EDGE('',*,*,#3810,.F.);
#5043=ORIENTED_EDGE('',*,*,#3811,.T.);
#5044=ORIENTED_EDGE('',*,*,#3812,.F.);
#5045=ORIENTED_EDGE('',*,*,#3813,.F.);
#5046=ORIENTED_EDGE('',*,*,#3814,.F.);
#5047=ORIENTED_EDGE('',*,*,#3815,.F.);
#5048=ORIENTED_EDGE('',*,*,#3816,.F.);
#5049=ORIENTED_EDGE('',*,*,#3817,.T.);
#5050=ORIENTED_EDGE('',*,*,#3818,.F.);
#5051=ORIENTED_EDGE('',*,*,#3817,.F.);
#5052=ORIENTED_EDGE('',*,*,#3819,.F.);
#5053=ORIENTED_EDGE('',*,*,#3811,.F.);
#5054=ORIENTED_EDGE('',*,*,#3815,.T.);
#5055=ORIENTED_EDGE('',*,*,#3820,.F.);
#5056=ORIENTED_EDGE('',*,*,#3813,.T.);
#5057=ORIENTED_EDGE('',*,*,#3821,.F.);
#5058=ORIENTED_EDGE('',*,*,#3822,.F.);
#5059=ORIENTED_EDGE('',*,*,#3823,.T.);
#5060=ORIENTED_EDGE('',*,*,#3824,.F.);
#5061=ORIENTED_EDGE('',*,*,#3823,.F.);
#5062=ORIENTED_EDGE('',*,*,#3825,.T.);
#5063=ORIENTED_EDGE('',*,*,#3821,.T.);
#5064=ORIENTED_EDGE('',*,*,#3812,.T.);
#5065=ORIENTED_EDGE('',*,*,#3819,.T.);
#5066=ORIENTED_EDGE('',*,*,#3816,.T.);
#5067=ORIENTED_EDGE('',*,*,#3820,.T.);
#5068=ORIENTED_EDGE('',*,*,#3814,.T.);
#5069=ORIENTED_EDGE('',*,*,#3818,.T.);
#5070=ORIENTED_EDGE('',*,*,#3810,.T.);
#5071=ORIENTED_EDGE('',*,*,#3822,.T.);
#5072=ORIENTED_EDGE('',*,*,#3825,.F.);
#5073=ORIENTED_EDGE('',*,*,#3826,.F.);
#5074=ORIENTED_EDGE('',*,*,#3827,.T.);
#5075=ORIENTED_EDGE('',*,*,#3824,.T.);
#5076=ORIENTED_EDGE('',*,*,#3827,.F.);
#5077=ORIENTED_EDGE('',*,*,#3826,.T.);
#5659=CYLINDRICAL_SURFACE('',#6984,0.175);
#5660=CYLINDRICAL_SURFACE('',#6985,0.1);
#5935=ADVANCED_FACE('',(#1036),#709,.F.);
#5936=ADVANCED_FACE('',(#1037),#710,.F.);
#5937=ADVANCED_FACE('',(#1038),#711,.F.);
#5938=ADVANCED_FACE('',(#1039),#712,.F.);
#5939=ADVANCED_FACE('',(#1040),#713,.F.);
#5940=ADVANCED_FACE('',(#1041,#529),#714,.T.);
#5941=ADVANCED_FACE('',(#1042),#5659,.T.);
#5942=ADVANCED_FACE('',(#1043),#5660,.T.);
#5943=ADVANCED_FACE('',(#1044),#715,.T.);
#6090=CLOSED_SHELL('',(#5935,#5936,#5937,#5938,#5939,#5940,#5941,#5942,
#5943));
#6970=AXIS2_PLACEMENT_3D('',#10732,#8449,#8450);
#6971=AXIS2_PLACEMENT_3D('',#10733,#8451,#8452);
#6972=AXIS2_PLACEMENT_3D('',#10742,#8457,#8458);
#6973=AXIS2_PLACEMENT_3D('',#10751,#8463,#8464);
#6974=AXIS2_PLACEMENT_3D('',#10752,#8465,#8466);
#6975=AXIS2_PLACEMENT_3D('',#10753,#8467,#8468);
#6976=AXIS2_PLACEMENT_3D('',#10754,#8469,#8470);
#6977=AXIS2_PLACEMENT_3D('',#10755,#8471,#8472);
#6978=AXIS2_PLACEMENT_3D('',#10756,#8473,#8474);
#6979=AXIS2_PLACEMENT_3D('',#10758,#8475,#8476);
#6980=AXIS2_PLACEMENT_3D('',#10759,#8477,#8478);
#6981=AXIS2_PLACEMENT_3D('',#10760,#8479,#8480);
#6982=AXIS2_PLACEMENT_3D('',#10762,#8481,#8482);
#6983=AXIS2_PLACEMENT_3D('',#10764,#8483,#8484);
#6984=AXIS2_PLACEMENT_3D('',#10765,#8485,#8486);
#6985=AXIS2_PLACEMENT_3D('',#10767,#8488,#8489);
#6986=AXIS2_PLACEMENT_3D('',#10769,#8490,#8491);
#6987=AXIS2_PLACEMENT_3D('',#10771,#8493,#8494);
#8449=DIRECTION('axis',(0.,0.,1.));
#8450=DIRECTION('refdir',(1.,0.,0.));
#8451=DIRECTION('center_axis',(-1.,0.,0.));
#8452=DIRECTION('ref_axis',(0.,0.,1.));
#8453=DIRECTION('',(0.,-1.,0.));
#8454=DIRECTION('',(0.,0.,1.));
#8455=DIRECTION('',(0.,1.,0.));
#8456=DIRECTION('',(0.,0.,1.));
#8457=DIRECTION('center_axis',(1.,0.,0.));
#8458=DIRECTION('ref_axis',(0.,0.,-1.));
#8459=DIRECTION('',(0.,1.,0.));
#8460=DIRECTION('',(0.,0.,-1.));
#8461=DIRECTION('',(0.,-1.,0.));
#8462=DIRECTION('',(0.,0.,-1.));
#8463=DIRECTION('center_axis',(0.,1.,0.));
#8464=DIRECTION('ref_axis',(0.,0.,1.));
#8465=DIRECTION('center_axis',(0.,1.,0.));
#8466=DIRECTION('ref_axis',(1.,0.,0.));
#8467=DIRECTION('center_axis',(0.,1.,0.));
#8468=DIRECTION('ref_axis',(1.,0.,0.));
#8469=DIRECTION('center_axis',(0.,1.,0.));
#8470=DIRECTION('ref_axis',(1.,0.,0.));
#8471=DIRECTION('center_axis',(0.,1.,0.));
#8472=DIRECTION('ref_axis',(1.,0.,0.));
#8473=DIRECTION('center_axis',(0.,1.,0.));
#8474=DIRECTION('ref_axis',(1.,0.,0.));
#8475=DIRECTION('center_axis',(0.,1.,0.));
#8476=DIRECTION('ref_axis',(1.,0.,0.));
#8477=DIRECTION('center_axis',(0.,1.,0.));
#8478=DIRECTION('ref_axis',(1.,0.,0.));
#8479=DIRECTION('center_axis',(0.,1.,0.));
#8480=DIRECTION('ref_axis',(1.,0.,0.));
#8481=DIRECTION('center_axis',(0.,1.,0.));
#8482=DIRECTION('ref_axis',(1.,0.,0.));
#8483=DIRECTION('center_axis',(0.,1.,0.));
#8484=DIRECTION('ref_axis',(1.,0.,0.));
#8485=DIRECTION('center_axis',(0.,1.,0.));
#8486=DIRECTION('ref_axis',(1.,0.,0.));
#8487=DIRECTION('',(0.,-1.,0.));
#8488=DIRECTION('center_axis',(0.,1.,0.));
#8489=DIRECTION('ref_axis',(1.,0.,0.));
#8490=DIRECTION('center_axis',(0.,1.,0.));
#8491=DIRECTION('ref_axis',(1.,0.,0.));
#8492=DIRECTION('',(0.,-1.,0.));
#8493=DIRECTION('center_axis',(0.,1.,0.));
#8494=DIRECTION('ref_axis',(1.,0.,0.));
#10732=CARTESIAN_POINT('',(0.,0.,0.));
#10733=CARTESIAN_POINT('Origin',(-0.83,-3.4,13.));
#10734=CARTESIAN_POINT('',(-0.83,-3.2,13.0275906035043));
#10735=CARTESIAN_POINT('',(-0.83,-3.3,13.0275906035043));
#10736=CARTESIAN_POINT('',(-0.83,-3.3,13.0275906035043));
#10737=CARTESIAN_POINT('',(-0.83,-3.2,13.3724093964957));
#10738=CARTESIAN_POINT('',(-0.83,-3.2,13.4));
#10739=CARTESIAN_POINT('',(-0.83,-3.3,13.3724093964957));
#10740=CARTESIAN_POINT('',(-0.83,-3.3,13.3724093964957));
#10741=CARTESIAN_POINT('',(-0.83,-3.3,13.1));
#10742=CARTESIAN_POINT('Origin',(-0.77,-3.4,13.4));
#10743=CARTESIAN_POINT('',(-0.77,-3.3,13.0275906035043));
#10744=CARTESIAN_POINT('',(-0.77,-3.2,13.0275906035043));
#10745=CARTESIAN_POINT('',(-0.77,-3.3,13.0275906035043));
#10746=CARTESIAN_POINT('',(-0.77,-3.3,13.3724093964957));
#10747=CARTESIAN_POINT('',(-0.77,-3.3,13.3));
#10748=CARTESIAN_POINT('',(-0.77,-3.2,13.3724093964957));
#10749=CARTESIAN_POINT('',(-0.77,-3.3,13.3724093964957));
#10750=CARTESIAN_POINT('',(-0.77,-3.2,13.));
#10751=CARTESIAN_POINT('Origin',(-0.8,-3.2,13.2));
#10752=CARTESIAN_POINT('Origin',(-0.8,-3.2,13.2));
#10753=CARTESIAN_POINT('Origin',(-0.8,-3.2,13.2));
#10754=CARTESIAN_POINT('Origin',(-0.8,-3.3,13.2));
#10755=CARTESIAN_POINT('Origin',(-0.8,-3.3,13.2));
#10756=CARTESIAN_POINT('Origin',(-0.8,-3.3,13.2));
#10757=CARTESIAN_POINT('',(-0.975,-3.3,13.2));
#10758=CARTESIAN_POINT('Origin',(-0.8,-3.3,13.2));
#10759=CARTESIAN_POINT('Origin',(-0.8,-3.3,13.2));
#10760=CARTESIAN_POINT('Origin',(-0.8,-3.1,13.2));
#10761=CARTESIAN_POINT('',(-0.975,-3.1,13.2));
#10762=CARTESIAN_POINT('Origin',(-0.8,-3.1,13.2));
#10763=CARTESIAN_POINT('',(-0.9,-3.1,13.2));
#10764=CARTESIAN_POINT('Origin',(-0.8,-3.1,13.2));
#10765=CARTESIAN_POINT('Origin',(-0.8,-3.3,13.2));
#10766=CARTESIAN_POINT('',(-0.975,-3.3,13.2));
#10767=CARTESIAN_POINT('Origin',(-0.8,-3.1,13.2));
#10768=CARTESIAN_POINT('',(-0.9,-2.1,13.2));
#10769=CARTESIAN_POINT('Origin',(-0.8,-2.1,13.2));
#10770=CARTESIAN_POINT('',(-0.9,-3.1,13.2));
#10771=CARTESIAN_POINT('Origin',(-0.8,-2.1,13.2));
#11379=UNCERTAINTY_MEASURE_WITH_UNIT(LENGTH_MEASURE(0.001),#11433,
'DISTANCE_ACCURACY_VALUE',
'Maximum model space distance between geometric entities at asserted c
onnectivities');
#11393=UNCERTAINTY_MEASURE_WITH_UNIT(LENGTH_MEASURE(0.001),#11433,
'DISTANCE_ACCURACY_VALUE',
'Maximum model space distance between geometric entities at asserted c
onnectivities');
#11418=(
GEOMETRIC_REPRESENTATION_CONTEXT(3)
GLOBAL_UNCERTAINTY_ASSIGNED_CONTEXT((#11379))
GLOBAL_UNIT_ASSIGNED_CONTEXT((#11433,#11435,#11436))
REPRESENTATION_CONTEXT('','3D')
);
#11432=(
GEOMETRIC_REPRESENTATION_CONTEXT(3)
GLOBAL_UNCERTAINTY_ASSIGNED_CONTEXT((#11393))
GLOBAL_UNIT_ASSIGNED_CONTEXT((#11433,#11435,#11436))
REPRESENTATION_CONTEXT('','3D')
);
#11433=(
LENGTH_UNIT()
NAMED_UNIT(*)
SI_UNIT(.CENTI.,.METRE.)
);
#11435=(
NAMED_UNIT(*)
PLANE_ANGLE_UNIT()
SI_UNIT($,.RADIAN.)
);
#11436=(
NAMED_UNIT(*)
SI_UNIT($,.STERADIAN.)
SOLID_ANGLE_UNIT()
);
#11461=SHAPE_DEFINITION_REPRESENTATION(#11499,#11587);
#11499=PRODUCT_DEFINITION_SHAPE('',$,#11626);
#11587=SHAPE_REPRESENTATION('',(#6970),#11418);
#11601=PRODUCT_DEFINITION_CONTEXT('part definition',#11717,'design');
#11626=PRODUCT_DEFINITION('M2 sight screw (1)',
'M2 sight screw (1)',#11664,#11601);
#11664=PRODUCT_DEFINITION_FORMATION('',$,#11743);
#11717=APPLICATION_CONTEXT(
'Core Data for Automotive Mechanical Design Process');
#11718=PRODUCT_CONTEXT('part definition',#11717,'mechanical');
#11743=PRODUCT('M2 sight screw (1)','M2 sight screw (1)',
'M2 sight screw (1)',(#11718));
#11820=COLOUR_RGB('Black',0.12,0.14,0.17);
#11821=FILL_AREA_STYLE_COLOUR('',#11820);
#11822=FILL_AREA_STYLE('',(#11821));
#11823=SURFACE_STYLE_FILL_AREA(#11822);
#11824=SURFACE_SIDE_STYLE('',(#11823));
#11825=SURFACE_STYLE_USAGE(.BOTH.,#11824);
#11826=PRESENTATION_STYLE_ASSIGNMENT((#11825));
ENDSEC;
END-ISO-10303-21;
